ISO-10303-21;
HEADER;
/* Generated by software containing ST-Developer
 * from STEP Tools, Inc. (www.steptools.com) 
 */

FILE_DESCRIPTION(
/* description */ ('XY cross-slide table'),
/* implementation_level */ '2;1');

FILE_NAME(
/* name */ 'Flat Washer - M5 (1).step',
/* time_stamp */ '2026-10-28T03:22:46-07:00',
/* author */ (''),
/* organization */ (''),
/* preprocessor_version */ 'ST-DEVELOPER v20.2',
/* originating_system */ 'Autodesk Translation Framework v15.17.0.0',
/* authorisation */ '');

FILE_SCHEMA (('AUTOMOTIVE_DESIGN { 1 0 10303 214 3 1 1 }'));
ENDSEC;

DATA;
#10=MECHANICAL_DESIGN_GEOMETRIC_PRESENTATION_REPRESENTATION('',(#1768),#62984);
#1478=CONICAL_SURFACE('',#25971,0.275,0.785398163397449);
#1572=SHAPE_REPRESENTATION_RELATIONSHIP('SRR','None',#63431,#1655);
#1655=ADVANCED_BREP_SHAPE_REPRESENTATION('',(#1876),#62968);
#1768=STYLED_ITEM('',(#63919),#1876);
#1876=MANIFOLD_SOLID_BREP('Body1',#23067);
#2257=FACE_BOUND('',#5564,.T.);
#2258=FACE_BOUND('',#5567,.T.);
#2769=PLANE('',#25976);
#2770=PLANE('',#25980);
#3877=FACE_OUTER_BOUND('',#5561,.T.);
#3878=FACE_OUTER_BOUND('',#5562,.T.);
#3879=FACE_OUTER_BOUND('',#5563,.T.);
#3880=FACE_OUTER_BOUND('',#5565,.T.);
#3881=FACE_OUTER_BOUND('',#5566,.T.);
#5561=EDGE_LOOP('',(#19530,#19531,#19532,#19533));
#5562=EDGE_LOOP('',(#19534,#19535,#19536,#19537));
#5563=EDGE_LOOP('',(#19538));
#5564=EDGE_LOOP('',(#19539));
#5565=EDGE_LOOP('',(#19540,#19541,#19542,#19543));
#5566=EDGE_LOOP('',(#19544));
#5567=EDGE_LOOP('',(#19545));
#7052=LINE('',#50173,#8539);
#7053=LINE('',#50177,#8540);
#7054=LINE('',#50184,#8541);
#8539=VECTOR('',#31553,0.275);
#8540=VECTOR('',#31558,0.265);
#8541=VECTOR('',#31567,0.5);
#9671=CIRCLE('',#25972,0.285);
#9672=CIRCLE('',#25973,0.265);
#9673=CIRCLE('',#25975,0.265);
#9674=CIRCLE('',#25977,0.5);
#9675=CIRCLE('',#25979,0.5);
#11338=VERTEX_POINT('',#50170);
#11339=VERTEX_POINT('',#50172);
#11340=VERTEX_POINT('',#50176);
#11341=VERTEX_POINT('',#50180);
#11342=VERTEX_POINT('',#50183);
#14149=EDGE_CURVE('',#11338,#11338,#9671,.T.);
#14150=EDGE_CURVE('',#11338,#11339,#7052,.T.);
#14151=EDGE_CURVE('',#11339,#11339,#9672,.T.);
#14152=EDGE_CURVE('',#11339,#11340,#7053,.T.);
#14153=EDGE_CURVE('',#11340,#11340,#9673,.T.);
#14154=EDGE_CURVE('',#11341,#11341,#9674,.T.);
#14155=EDGE_CURVE('',#11341,#11342,#7054,.T.);
#14156=EDGE_CURVE('',#11342,#11342,#9675,.T.);
#19530=ORIENTED_EDGE('',*,*,#14149,.T.);
#19531=ORIENTED_EDGE('',*,*,#14150,.T.);
#19532=ORIENTED_EDGE('',*,*,#14151,.T.);
#19533=ORIENTED_EDGE('',*,*,#14150,.F.);
#19534=ORIENTED_EDGE('',*,*,#14151,.F.);
#19535=ORIENTED_EDGE('',*,*,#14152,.T.);
#19536=ORIENTED_EDGE('',*,*,#14153,.T.);
#19537=ORIENTED_EDGE('',*,*,#14152,.F.);
#19538=ORIENTED_EDGE('',*,*,#14154,.T.);
#19539=ORIENTED_EDGE('',*,*,#14149,.F.);
#19540=ORIENTED_EDGE('',*,*,#14154,.F.);
#19541=ORIENTED_EDGE('',*,*,#14155,.T.);
#19542=ORIENTED_EDGE('',*,*,#14156,.T.);
#19543=ORIENTED_EDGE('',*,*,#14155,.F.);
#19544=ORIENTED_EDGE('',*,*,#14156,.F.);
#19545=ORIENTED_EDGE('',*,*,#14153,.F.);
#21466=CYLINDRICAL_SURFACE('',#25974,0.265);
#21467=CYLINDRICAL_SURFACE('',#25978,0.5);
#22658=ADVANCED_FACE('',(#3877),#1478,.F.);
#22659=ADVANCED_FACE('',(#3878),#21466,.F.);
#22660=ADVANCED_FACE('',(#3879,#2257),#2769,.T.);
#22661=ADVANCED_FACE('',(#3880),#21467,.T.);
#22662=ADVANCED_FACE('',(#3881,#2258),#2770,.F.);
#23067=CLOSED_SHELL('',(#22658,#22659,#22660,#22661,#22662));
#25970=AXIS2_PLACEMENT_3D('',#50168,#31547,#31548);
#25971=AXIS2_PLACEMENT_3D('',#50169,#31549,#31550);
#25972=AXIS2_PLACEMENT_3D('',#50171,#31551,#31552);
#25973=AXIS2_PLACEMENT_3D('',#50174,#31554,#31555);
#25974=AXIS2_PLACEMENT_3D('',#50175,#31556,#31557);
#25975=AXIS2_PLACEMENT_3D('',#50178,#31559,#31560);
#25976=AXIS2_PLACEMENT_3D('',#50179,#31561,#31562);
#25977=AXIS2_PLACEMENT_3D('',#50181,#31563,#31564);
#25978=AXIS2_PLACEMENT_3D('',#50182,#31565,#31566);
#25979=AXIS2_PLACEMENT_3D('',#50185,#31568,#31569);
#25980=AXIS2_PLACEMENT_3D('',#50186,#31570,#31571);
#31547=DIRECTION('axis',(0.,0.,1.));
#31548=DIRECTION('refdir',(1.,0.,0.));
#31549=DIRECTION('center_axis',(0.,1.,0.));
#31550=DIRECTION('ref_axis',(1.,0.,0.));
#31551=DIRECTION('center_axis',(0.,1.,0.));
#31552=DIRECTION('ref_axis',(1.,0.,0.));
#31553=DIRECTION('',(0.707106781186548,-0.707106781186547,-8.65956056235494E-17));
#31554=DIRECTION('center_axis',(0.,-1.,0.));
#31555=DIRECTION('ref_axis',(1.,0.,0.));
#31556=DIRECTION('center_axis',(0.,1.,0.));
#31557=DIRECTION('ref_axis',(1.,0.,0.));
#31558=DIRECTION('',(0.,-1.,0.));
#31559=DIRECTION('center_axis',(0.,-1.,0.));
#31560=DIRECTION('ref_axis',(1.,0.,0.));
#31561=DIRECTION('center_axis',(0.,1.,0.));
#31562=DIRECTION('ref_axis',(1.,0.,0.));
#31563=DIRECTION('center_axis',(0.,1.,0.));
#31564=DIRECTION('ref_axis',(1.,0.,0.));
#31565=DIRECTION('center_axis',(0.,1.,0.));
#31566=DIRECTION('ref_axis',(1.,0.,0.));
#31567=DIRECTION('',(0.,-1.,0.));
#31568=DIRECTION('center_axis',(0.,1.,0.));
#31569=DIRECTION('ref_axis',(1.,0.,0.));
#31570=DIRECTION('center_axis',(0.,1.,0.));
#31571=DIRECTION('ref_axis',(1.,0.,0.));
#50168=CARTESIAN_POINT('',(0.,0.,0.));
#50169=CARTESIAN_POINT('Origin',(0.,0.09,0.));
#50170=CARTESIAN_POINT('',(-0.285,0.1,3.49024337756996E-17));
#50171=CARTESIAN_POINT('Origin',(0.,0.1,0.));
#50172=CARTESIAN_POINT('',(-0.265,0.08,-3.24531401774049E-17));
#50173=CARTESIAN_POINT('',(-0.275,0.09,3.36777869765522E-17));
#50174=CARTESIAN_POINT('Origin',(0.,0.08,0.));
#50175=CARTESIAN_POINT('Origin',(0.,0.,0.));
#50176=CARTESIAN_POINT('',(-0.265,0.,3.24531401774049E-17));
#50177=CARTESIAN_POINT('',(-0.265,0.,3.24531401774049E-17));
#50178=CARTESIAN_POINT('Origin',(0.,0.,0.));
#50179=CARTESIAN_POINT('Origin',(0.,0.1,0.));
#50180=CARTESIAN_POINT('',(-0.5,0.1,6.12323399573677E-17));
#50181=CARTESIAN_POINT('Origin',(0.,0.1,0.));
#50182=CARTESIAN_POINT('Origin',(0.,0.,0.));
#50183=CARTESIAN_POINT('',(-0.5,0.,6.12323399573677E-17));
#50184=CARTESIAN_POINT('',(-0.5,0.,6.12323399573677E-17));
#50185=CARTESIAN_POINT('Origin',(0.,0.,0.));
#50186=CARTESIAN_POINT('Origin',(0.,0.,0.));
#62869=UNCERTAINTY_MEASURE_WITH_UNIT(LENGTH_MEASURE(0.001),#62985,
'DISTANCE_ACCURACY_VALUE',
'Maximum model space distance between geometric entities at asserted c
onnectivities');
#62885=UNCERTAINTY_MEASURE_WITH_UNIT(LENGTH_MEASURE(0.001),#62985,
'DISTANCE_ACCURACY_VALUE',
'Maximum model space distance between geometric entities at asserted c
onnectivities');
#62968=(
GEOMETRIC_REPRESENTATION_CONTEXT(3)
GLOBAL_UNCERTAINTY_ASSIGNED_CONTEXT((#62869))
GLOBAL_UNIT_ASSIGNED_CONTEXT((#62985,#62987,#62988))
REPRESENTATION_CONTEXT('','3D')
);
#62984=(
GEOMETRIC_REPRESENTATION_CONTEXT(3)
GLOBAL_UNCERTAINTY_ASSIGNED_CONTEXT((#62885))
GLOBAL_UNIT_ASSIGNED_CONTEXT((#62985,#62987,#62988))
REPRESENTATION_CONTEXT('','3D')
);
#62985=(
LENGTH_UNIT()
NAMED_UNIT(*)
SI_UNIT(.CENTI.,.METRE.)
);
#62987=(
NAMED_UNIT(*)
PLANE_ANGLE_UNIT()
SI_UNIT($,.RADIAN.)
);
#62988=(
NAMED_UNIT(*)
SI_UNIT($,.STERADIAN.)
SOLID_ANGLE_UNIT()
);
#63071=SHAPE_DEFINITION_REPRESENTATION(#63262,#63431);
#63262=PRODUCT_DEFINITION_SHAPE('',$,#63530);
#63431=SHAPE_REPRESENTATION('',(#25970),#62968);
#63447=PRODUCT_DEFINITION_CONTEXT('part definition',#63743,'design');
#63530=PRODUCT_DEFINITION('Flat Washer - M5 (1)','Flat Washer - M5 (1)',#63628,
#63447);
#63628=PRODUCT_DEFINITION_FORMATION('',$,#63827);
#63743=APPLICATION_CONTEXT(
'Core Data for Automotive Mechanical Design Process');
#63744=PRODUCT_CONTEXT('part definition',#63743,'mechanical');
#63827=PRODUCT('Flat Washer - M5 (1)','Flat Washer - M5 (1)',
'Flat Washer - M5 (1)',(#63744));
#63913=COLOUR_RGB('Black',0.12,0.14,0.17);
#63914=FILL_AREA_STYLE_COLOUR('',#63913);
#63915=FILL_AREA_STYLE('',(#63914));
#63916=SURFACE_STYLE_FILL_AREA(#63915);
#63917=SURFACE_SIDE_STYLE('',(#63916));
#63918=SURFACE_STYLE_USAGE(.BOTH.,#63917);
#63919=PRESENTATION_STYLE_ASSIGNMENT((#63918));
ENDSEC;
END-ISO-10303-21;
